ISO-10303-21;
HEADER;
/* Generated by software containing ST-Developer
 * from STEP Tools, Inc. (www.steptools.com) 
 */

FILE_DESCRIPTION(
/* description */ ('PAT-091'),
/* implementation_level */ '2;1');

FILE_NAME(
/* name */ 'Guide shaft (2).step',
/* time_stamp */ '2026-10-27T15:34:44-07:00',
/* author */ (''),
/* organization */ (''),
/* preprocessor_version */ 'ST-DEVELOPER v20.2',
/* originating_system */ 'Autodesk Translation Framework v15.17.0.0',
/* authorisation */ '');

FILE_SCHEMA (('AUTOMOTIVE_DESIGN { 1 0 10303 214 3 1 1 }'));
ENDSEC;

DATA;
#10=MECHANICAL_DESIGN_GEOMETRIC_PRESENTATION_REPRESENTATION('',(#992),#25100);
#772=SHAPE_REPRESENTATION_RELATIONSHIP('SRR','None',#25534,#882);
#882=ADVANCED_BREP_SHAPE_REPRESENTATION('',(#1115),#25004);
#992=STYLED_ITEM('',(#26191),#1115);
#1115=MANIFOLD_SOLID_BREP('Body1',#13270);
#1746=PLANE('',#15016);
#1747=PLANE('',#15017);
#2269=FACE_OUTER_BOUND('',#3249,.T.);
#2270=FACE_OUTER_BOUND('',#3250,.T.);
#2271=FACE_OUTER_BOUND('',#3251,.T.);
#3249=EDGE_LOOP('',(#9890,#9891,#9892,#9893));
#3250=EDGE_LOOP('',(#9894));
#3251=EDGE_LOOP('',(#9895));
#4386=LINE('',#21973,#5126);
#5126=VECTOR('',#17590,0.6);
#5801=CIRCLE('',#15014,0.6);
#5802=CIRCLE('',#15015,0.6);
#6688=VERTEX_POINT('',#21970);
#6689=VERTEX_POINT('',#21972);
#7880=EDGE_CURVE('',#6688,#6688,#5801,.T.);
#7881=EDGE_CURVE('',#6688,#6689,#4386,.T.);
#7882=EDGE_CURVE('',#6689,#6689,#5802,.T.);
#9890=ORIENTED_EDGE('',*,*,#7880,.F.);
#9891=ORIENTED_EDGE('',*,*,#7881,.T.);
#9892=ORIENTED_EDGE('',*,*,#7882,.T.);
#9893=ORIENTED_EDGE('',*,*,#7881,.F.);
#9894=ORIENTED_EDGE('',*,*,#7880,.T.);
#9895=ORIENTED_EDGE('',*,*,#7882,.F.);
#12171=CYLINDRICAL_SURFACE('',#15013,0.6);
#12636=ADVANCED_FACE('',(#2269),#12171,.T.);
#12637=ADVANCED_FACE('',(#2270),#1746,.T.);
#12638=ADVANCED_FACE('',(#2271),#1747,.F.);
#13270=CLOSED_SHELL('',(#12636,#12637,#12638));
#15012=AXIS2_PLACEMENT_3D('',#21968,#17584,#17585);
#15013=AXIS2_PLACEMENT_3D('',#21969,#17586,#17587);
#15014=AXIS2_PLACEMENT_3D('',#21971,#17588,#17589);
#15015=AXIS2_PLACEMENT_3D('',#21974,#17591,#17592);
#15016=AXIS2_PLACEMENT_3D('',#21975,#17593,#17594);
#15017=AXIS2_PLACEMENT_3D('',#21976,#17595,#17596);
#17584=DIRECTION('axis',(0.,0.,1.));
#17585=DIRECTION('refdir',(1.,0.,0.));
#17586=DIRECTION('center_axis',(1.,0.,0.));
#17587=DIRECTION('ref_axis',(0.,0.,-1.));
#17588=DIRECTION('center_axis',(1.,0.,0.));
#17589=DIRECTION('ref_axis',(0.,0.,-1.));
#17590=DIRECTION('',(-1.,0.,0.));
#17591=DIRECTION('center_axis',(1.,0.,0.));
#17592=DIRECTION('ref_axis',(0.,0.,-1.));
#17593=DIRECTION('center_axis',(1.,0.,0.));
#17594=DIRECTION('ref_axis',(0.,0.,-1.));
#17595=DIRECTION('center_axis',(1.,0.,0.));
#17596=DIRECTION('ref_axis',(0.,0.,-1.));
#21968=CARTESIAN_POINT('',(0.,0.,0.));
#21969=CARTESIAN_POINT('Origin',(-1.,-3.,16.));
#21970=CARTESIAN_POINT('',(47.,-3.,16.6));
#21971=CARTESIAN_POINT('Origin',(47.,-3.,16.));
#21972=CARTESIAN_POINT('',(-1.,-3.,16.6));
#21973=CARTESIAN_POINT('',(-1.,-3.,16.6));
#21974=CARTESIAN_POINT('Origin',(-1.,-3.,16.));
#21975=CARTESIAN_POINT('Origin',(47.,-3.,16.));
#21976=CARTESIAN_POINT('Origin',(-1.,-3.,16.));
#24883=UNCERTAINTY_MEASURE_WITH_UNIT(LENGTH_MEASURE(0.001),#25101,
'DISTANCE_ACCURACY_VALUE',
'Maximum model space distance between geometric entities at asserted c
onnectivities');
#24979=UNCERTAINTY_MEASURE_WITH_UNIT(LENGTH_MEASURE(0.001),#25101,
'DISTANCE_ACCURACY_VALUE',
'Maximum model space distance between geometric entities at asserted c
onnectivities');
#25004=(
GEOMETRIC_REPRESENTATION_CONTEXT(3)
GLOBAL_UNCERTAINTY_ASSIGNED_CONTEXT((#24883))
GLOBAL_UNIT_ASSIGNED_CONTEXT((#25101,#25103,#25104))
REPRESENTATION_CONTEXT('','3D')
);
#25100=(
GEOMETRIC_REPRESENTATION_CONTEXT(3)
GLOBAL_UNCERTAINTY_ASSIGNED_CONTEXT((#24979))
GLOBAL_UNIT_ASSIGNED_CONTEXT((#25101,#25103,#25104))
REPRESENTATION_CONTEXT('','3D')
);
#25101=(
LENGTH_UNIT()
NAMED_UNIT(*)
SI_UNIT(.CENTI.,.METRE.)
);
#25103=(
NAMED_UNIT(*)
PLANE_ANGLE_UNIT()
SI_UNIT($,.RADIAN.)
);
#25104=(
NAMED_UNIT(*)
SI_UNIT($,.STERADIAN.)
SOLID_ANGLE_UNIT()
);
#25129=SHAPE_DEFINITION_REPRESENTATION(#25249,#25534);
#25249=PRODUCT_DEFINITION_SHAPE('',$,#25655);
#25534=SHAPE_REPRESENTATION('',(#15012),#25004);
#25630=PRODUCT_DEFINITION_CONTEXT('part definition',#25992,'design');
#25655=PRODUCT_DEFINITION('Guide shaft (2)','Guide shaft (2)',#25775,#25630);
#25775=PRODUCT_DEFINITION_FORMATION('',$,#26018);
#25992=APPLICATION_CONTEXT(
'Core Data for Automotive Mechanical Design Process');
#25993=PRODUCT_CONTEXT('part definition',#25992,'mechanical');
#26018=PRODUCT('Guide shaft (2)','Guide shaft (2)','Guide shaft (2)',(#25993));
#26185=COLOUR_RGB('Grey',0.48,0.52,0.57);
#26186=FILL_AREA_STYLE_COLOUR('',#26185);
#26187=FILL_AREA_STYLE('',(#26186));
#26188=SURFACE_STYLE_FILL_AREA(#26187);
#26189=SURFACE_SIDE_STYLE('',(#26188));
#26190=SURFACE_STYLE_USAGE(.BOTH.,#26189);
#26191=PRESENTATION_STYLE_ASSIGNMENT((#26190));
ENDSEC;
END-ISO-10303-21;
